ISO-10303-21;
HEADER;
FILE_DESCRIPTION (('STEP AP203'),
    '1' );
FILE_NAME ('1602p_c_21.step',
    '2026-10-31T14:11:27',
    ( '' ),
    ( '' ),
    'SwSTEP 2.0',
    'SolidWorks 2024',
    '' );
FILE_SCHEMA (( 'AUTOMOTIVE_DESIGN' ));
ENDSEC;

DATA;
#5=CIRCLE ( 'NONE', #20894, 5.000000000000000000 ) ;
#97=CARTESIAN_POINT ( 'NONE',  ( -20.00000000397270128, 22.95208919256889857, -4.999999999995559996 ) ) ;
#296=DIRECTION ( 'NONE',  ( 1.751019220569994795E-16, 2.300154215587015208E-15, 1.000000000000000000 ) ) ;
#360=EDGE_LOOP ( 'NONE', ( #4752, #20568 ) ) ;
#415=DIRECTION ( 'NONE',  ( 1.000000000000000000, 0.000000000000000000, 0.000000000000000000 ) ) ;
#478=AXIS2_PLACEMENT_3D ( 'NONE', #21824, #14241, #10702 ) ;
#508=AXIS2_PLACEMENT_3D ( 'NONE', #18123, #10789, #12884 ) ;
#525=DIRECTION ( 'NONE',  ( -1.751019220569994795E-16, -2.300154215587015208E-15, -1.000000000000000000 ) ) ;
#739=CARTESIAN_POINT ( 'NONE',  ( -19.81505072009858992, 25.44523855881121577, -4.999999999995566213 ) ) ;
#1102=DIRECTION ( 'NONE',  ( 1.751019220569994795E-16, 2.300154215587015208E-15, 1.000000000000000000 ) ) ;
#1110=VERTEX_POINT ( 'NONE', #3371 ) ;
#1115=EDGE_LOOP ( 'NONE', ( #6960, #12459 ) ) ;
#1172=EDGE_LOOP ( 'NONE', ( #18340, #9582, #4866, #17239 ) ) ;
#1457=CLOSED_SHELL ( 'NONE', ( #4208, #17229, #17531, #19358, #21249, #2265 ) ) ;
#1482=EDGE_CURVE ( 'NONE', #14624, #2629, #9910, .T. ) ;
#1655=AXIS2_PLACEMENT_3D ( 'NONE', #10487, #12609, #19850 ) ;
#1756=PLANE ( 'NONE',  #13502 ) ;
#1812=EDGE_LOOP ( 'NONE', ( #6178, #4530 ) ) ;
#2265=ADVANCED_FACE ( 'NONE', ( #3664, #21714 ), #1756, .T. ) ;
#2329=DIRECTION ( 'NONE',  ( -0.07397971354964408275, -0.9972597464969258363, 2.255140518769849223E-15 ) ) ;
#2402=CIRCLE ( 'NONE', #11162, 2.500000000000000444 ) ;
#2536=EDGE_CURVE ( 'NONE', #14624, #1110, #11252, .T. ) ;
#2553=ADVANCED_BREP_SHAPE_REPRESENTATION ( '', ( #17389, #12739 ), #10500 ) ;
#2569=CARTESIAN_POINT ( 'NONE',  ( 0.000000000000000000, 0.000000000000000000, 0.000000000000000000 ) ) ;
#2577=EDGE_CURVE ( 'NONE', #20612, #14607, #14899, .T. ) ;
#2629=VERTEX_POINT ( 'NONE', #21063 ) ;
#2643=CYLINDRICAL_SURFACE ( 'NONE', #6583, 5.000000000000000000 ) ;
#2710=EDGE_CURVE ( 'NONE', #17907, #2629, #10123, .T. ) ;
#3249=UNCERTAINTY_MEASURE_WITH_UNIT (LENGTH_MEASURE( 1.000000000000000082E-05 ), #8484, 'distance_accuracy_value', 'NONE');
#3371=CARTESIAN_POINT ( 'NONE',  ( -19.63010143622448211, 27.93838792505352941, -4.999999999995571542 ) ) ;
#3508=DIRECTION ( 'NONE',  ( 1.751019220569994795E-16, 2.300154215587015208E-15, 1.000000000000000000 ) ) ;
#3664=FACE_BOUND ( 'NONE', #1812, .T. ) ;
#3684=VERTEX_POINT ( 'NONE', #17666 ) ;
#4024=AXIS2_PLACEMENT_3D ( 'NONE', #22243, #17025, #18721 ) ;
#4204=EDGE_CURVE ( 'NONE', #14607, #10212, #15662, .T. ) ;
#4208=ADVANCED_FACE ( 'NONE', ( #10283 ), #15727, .T. ) ;
#4427=CARTESIAN_POINT ( 'NONE',  ( -20.00000000397270128, 22.95208919256889857, -4.999999999995559996 ) ) ;
#4530=ORIENTED_EDGE ( 'NONE', *, *, #6919, .T. ) ;
#4752=ORIENTED_EDGE ( 'NONE', *, *, #2536, .T. ) ;
#4758=APPLICATION_CONTEXT ( 'configuration controlled 3d designs of mechanical parts and assemblies' ) ;
#4866=ORIENTED_EDGE ( 'NONE', *, *, #1482, .T. ) ;
#5420=AXIS2_PLACEMENT_3D ( 'NONE', #21067, #1102, #15606 ) ;
#5493=SHAPE_REPRESENTATION ( '1602p_c_21', ( #12739 ), #10500 ) ;
#5636=FACE_OUTER_BOUND ( 'NONE', #17401, .T. ) ;
#5837=VECTOR ( 'NONE', #8936, 1000.000000000000000 ) ;
#5877=DIRECTION ( 'NONE',  ( -1.751019220569994795E-16, -2.300154215587015208E-15, -1.000000000000000000 ) ) ;
#6178=ORIENTED_EDGE ( 'NONE', *, *, #21107, .T. ) ;
#6373=EDGE_CURVE ( 'NONE', #3684, #10212, #16278, .T. ) ;
#6431=ORIENTED_EDGE ( 'NONE', *, *, #4204, .F. ) ;
#6471=VECTOR ( 'NONE', #19278, 1000.000000000000000 ) ;
#6583=AXIS2_PLACEMENT_3D ( 'NONE', #4427, #22226, #16773 ) ;
#6820=CARTESIAN_POINT ( 'NONE',  ( -20.00000000397270128, 22.95208919256889857, -5.499999999995559996 ) ) ;
#6908=DIRECTION ( 'NONE',  ( 1.751019220569994795E-16, 2.300154215587015208E-15, 1.000000000000000000 ) ) ;
#6919=EDGE_CURVE ( 'NONE', #20612, #3684, #11127, .T. ) ;
#6947=AXIS2_PLACEMENT_3D ( 'NONE', #8253, #13944, #23069 ) ;
#6960=ORIENTED_EDGE ( 'NONE', *, *, #13730, .T. ) ;
#7132=AXIS2_PLACEMENT_3D ( 'NONE', #10074, #3508, #17881 ) ;
#7215=PRODUCT ( '1602p_c_21', '1602p_c_21', '', ( #11990 ) ) ;
#7317=DESIGN_CONTEXT ( 'detailed design', #4758, 'design' ) ;
#7503=CARTESIAN_POINT ( 'NONE',  ( -20.00000000397270128, 22.95208919256889857, -5.499999999995559996 ) ) ;
#7519=CARTESIAN_POINT ( 'NONE',  ( -19.81505072009858992, 25.44523855881121577, -5.499999999995565325 ) ) ;
#7783=ORIENTED_EDGE ( 'NONE', *, *, #6373, .T. ) ;
#7789=ORIENTED_EDGE ( 'NONE', *, *, #2710, .T. ) ;
#8253=CARTESIAN_POINT ( 'NONE',  ( -20.00000000397270128, 22.95208919256889857, -4.999999999995559996 ) ) ;
#8484=( LENGTH_UNIT ( ) NAMED_UNIT ( * ) SI_UNIT ( .MILLI., .METRE. ) );
#8552=ORIENTED_EDGE ( 'NONE', *, *, #2577, .F. ) ;
#8580=FACE_OUTER_BOUND ( 'NONE', #22104, .T. ) ;
#8600=DIRECTION ( 'NONE',  ( 1.751019220569994795E-16, 2.300154215587015208E-15, 1.000000000000000000 ) ) ;
#8936=DIRECTION ( 'NONE',  ( -1.751019220569994795E-16, -2.300154215587015208E-15, -1.000000000000000000 ) ) ;
#9164=FACE_OUTER_BOUND ( 'NONE', #11685, .T. ) ;
#9582=ORIENTED_EDGE ( 'NONE', *, *, #2536, .F. ) ;
#9910=LINE ( 'NONE', #17136, #6471 ) ;
#10005=EDGE_CURVE ( 'NONE', #1110, #14624, #5, .T. ) ;
#10074=CARTESIAN_POINT ( 'NONE',  ( -20.00000000397270128, 22.95208919256889857, -5.499999999995559996 ) ) ;
#10108=ORIENTED_EDGE ( 'NONE', *, *, #1482, .F. ) ;
#10123=CIRCLE ( 'NONE', #21483, 5.000000000000000000 ) ;
#10212=VERTEX_POINT ( 'NONE', #13737 ) ;
#10283=FACE_OUTER_BOUND ( 'NONE', #20564, .T. ) ;
#10308=VECTOR ( 'NONE', #525, 1000.000000000000000 ) ;
#10482=DIRECTION ( 'NONE',  ( -0.07397971354964408275, -0.9972597464969258363, 2.255140518769849223E-15 ) ) ;
#10487=CARTESIAN_POINT ( 'NONE',  ( -20.00000000397270128, 22.95208919256889857, -4.999999999995559996 ) ) ;
#10500=( GEOMETRIC_REPRESENTATION_CONTEXT ( 3 ) GLOBAL_UNCERTAINTY_ASSIGNED_CONTEXT ( ( #3249 ) ) GLOBAL_UNIT_ASSIGNED_CONTEXT ( ( #8484, #15476, #22702 ) ) REPRESENTATION_CONTEXT ( 'NONE', 'WORKASPACE' ) );
#10616=EDGE_CURVE ( 'NONE', #1110, #17907, #16913, .T. ) ;
#10702=DIRECTION ( 'NONE',  ( -0.07397971354964476276, -0.9972597464969256142, 2.428612866367529538E-15 ) ) ;
#10789=DIRECTION ( 'NONE',  ( -1.751019220569994795E-16, -2.300154215587015208E-15, -1.000000000000000000 ) ) ;
#11127=CIRCLE ( 'NONE', #478, 2.500000000000000444 ) ;
#11162=AXIS2_PLACEMENT_3D ( 'NONE', #13689, #20928, #21054 ) ;
#11252=CIRCLE ( 'NONE', #4024, 5.000000000000000000 ) ;
#11379=ORIENTED_EDGE ( 'NONE', *, *, #2710, .F. ) ;
#11452=CARTESIAN_POINT ( 'NONE',  ( -20.36989857172092044, 17.96579046008427127, -4.999999999995548450 ) ) ;
#11654=VECTOR ( 'NONE', #5877, 1000.000000000000000 ) ;
#11685=EDGE_LOOP ( 'NONE', ( #16519, #11379 ) ) ;
#11990=MECHANICAL_CONTEXT ( 'NONE', #19592, 'mechanical' ) ;
#12024=AXIS2_PLACEMENT_3D ( 'NONE', #7503, #12627, #17970 ) ;
#12459=ORIENTED_EDGE ( 'NONE', *, *, #4204, .T. ) ;
#12609=DIRECTION ( 'NONE',  ( -1.751019220569994795E-16, -2.300154215587015208E-15, -1.000000000000000000 ) ) ;
#12627=DIRECTION ( 'NONE',  ( 4.027614241767943373E-31, 2.300154215587010080E-15, 1.000000000000000000 ) ) ;
#12665=EDGE_CURVE ( 'NONE', #2629, #17907, #19938, .T. ) ;
#12731=ORIENTED_EDGE ( 'NONE', *, *, #10616, .T. ) ;
#12739=AXIS2_PLACEMENT_3D ( 'NONE', #2569, #13380, #415 ) ;
#12816=CIRCLE ( 'NONE', #7132, 2.500000000000000444 ) ;
#12840=CARTESIAN_POINT ( 'NONE',  ( -20.18494928784681264, 20.45893982632658492, -4.999999999995553779 ) ) ;
#12884=DIRECTION ( 'NONE',  ( -0.07397971354964476276, -0.9972597464969256142, 2.428612866367529538E-15 ) ) ;
#12958=FACE_BOUND ( 'NONE', #1115, .T. ) ;
#13199=ORIENTED_EDGE ( 'NONE', *, *, #13730, .F. ) ;
#13380=DIRECTION ( 'NONE',  ( 0.000000000000000000, 0.000000000000000000, 1.000000000000000000 ) ) ;
#13433=ORIENTED_EDGE ( 'NONE', *, *, #6919, .F. ) ;
#13502=AXIS2_PLACEMENT_3D ( 'NONE', #97, #19943, #14597 ) ;
#13689=CARTESIAN_POINT ( 'NONE',  ( -20.00000000397270128, 22.95208919256889857, -4.999999999995559996 ) ) ;
#13730=EDGE_CURVE ( 'NONE', #10212, #14607, #12816, .T. ) ;
#13737=CARTESIAN_POINT ( 'NONE',  ( -20.18494928784681264, 20.45893982632658492, -5.499999999995553779 ) ) ;
#13829=DIRECTION ( 'NONE',  ( -0.07397971354964408275, -0.9972597464969258363, 2.255140518769849223E-15 ) ) ;
#13944=DIRECTION ( 'NONE',  ( -1.751019220569994795E-16, -2.300154215587015208E-15, -1.000000000000000000 ) ) ;
#14241=DIRECTION ( 'NONE',  ( -1.751019220569994795E-16, -2.300154215587015208E-15, -1.000000000000000000 ) ) ;
#14430=CYLINDRICAL_SURFACE ( 'NONE', #508, 2.500000000000000444 ) ;
#14597=DIRECTION ( 'NONE',  ( 1.000000000000000000, -1.751019220569989865E-16, -7.006492321624090605E-47 ) ) ;
#14607=VERTEX_POINT ( 'NONE', #7519 ) ;
#14624=VERTEX_POINT ( 'NONE', #11452 ) ;
#14899=LINE ( 'NONE', #739, #11654 ) ;
#15476=( NAMED_UNIT ( * ) PLANE_ANGLE_UNIT ( ) SI_UNIT ( $, .RADIAN. ) );
#15606=DIRECTION ( 'NONE',  ( -0.07397971354964476276, -0.9972597464969256142, 2.428612866367529538E-15 ) ) ;
#15662=CIRCLE ( 'NONE', #5420, 2.500000000000000444 ) ;
#15718=SHAPE_REPRESENTATION_RELATIONSHIP ( 'NONE' , 'NONE' ,  #5493, #2553 ) ;
#15727=CYLINDRICAL_SURFACE ( 'NONE', #6947, 5.000000000000000000 ) ;
#15898=ORIENTED_EDGE ( 'NONE', *, *, #6373, .F. ) ;
#16188=ORIENTED_EDGE ( 'NONE', *, *, #2577, .T. ) ;
#16252=ORIENTED_EDGE ( 'NONE', *, *, #21107, .F. ) ;
#16278=LINE ( 'NONE', #12840, #5837 ) ;
#16519=ORIENTED_EDGE ( 'NONE', *, *, #12665, .F. ) ;
#16771=PRODUCT_DEFINITION ( 'UNKNOWN', '', #19398, #7317 ) ;
#16773=DIRECTION ( 'NONE',  ( -0.07397971354964408275, -0.9972597464969258363, 2.255140518769849223E-15 ) ) ;
#16891=FACE_OUTER_BOUND ( 'NONE', #1172, .T. ) ;
#16913=LINE ( 'NONE', #18939, #10308 ) ;
#17025=DIRECTION ( 'NONE',  ( 1.751019220569994795E-16, 2.300154215587015208E-15, 1.000000000000000000 ) ) ;
#17038=ORIENTED_EDGE ( 'NONE', *, *, #10005, .F. ) ;
#17136=CARTESIAN_POINT ( 'NONE',  ( -20.36989857172092044, 17.96579046008427127, -4.999999999995548450 ) ) ;
#17229=ADVANCED_FACE ( 'NONE', ( #5636 ), #14430, .F. ) ;
#17239=ORIENTED_EDGE ( 'NONE', *, *, #12665, .T. ) ;
#17389=MANIFOLD_SOLID_BREP ( 'Imported1', #1457 ) ;
#17401=EDGE_LOOP ( 'NONE', ( #13433, #16188, #13199, #15898 ) ) ;
#17433=PRODUCT_DEFINITION_SHAPE ( 'NONE', 'NONE',  #16771 ) ;
#17531=ADVANCED_FACE ( 'NONE', ( #8580 ), #19496, .F. ) ;
#17666=CARTESIAN_POINT ( 'NONE',  ( -20.18494928784681264, 20.45893982632658492, -4.999999999995553779 ) ) ;
#17881=DIRECTION ( 'NONE',  ( -0.07397971354964476276, -0.9972597464969256142, 2.428612866367529538E-15 ) ) ;
#17907=VERTEX_POINT ( 'NONE', #22308 ) ;
#17970=DIRECTION ( 'NONE',  ( 1.000000000000000000, -1.751019220569989865E-16, -7.006492321624090605E-47 ) ) ;
#18123=CARTESIAN_POINT ( 'NONE',  ( -20.00000000397270128, 22.95208919256889857, -4.999999999995559996 ) ) ;
#18340=ORIENTED_EDGE ( 'NONE', *, *, #10616, .F. ) ;
#18721=DIRECTION ( 'NONE',  ( -0.07397971354964408275, -0.9972597464969258363, 2.255140518769849223E-15 ) ) ;
#18939=CARTESIAN_POINT ( 'NONE',  ( -19.63010143622448211, 27.93838792505352941, -4.999999999995571542 ) ) ;
#19278=DIRECTION ( 'NONE',  ( -1.751019220569994795E-16, -2.300154215587015208E-15, -1.000000000000000000 ) ) ;
#19358=ADVANCED_FACE ( 'NONE', ( #16891 ), #2643, .T. ) ;
#19398=PRODUCT_DEFINITION_FORMATION_WITH_SPECIFIED_SOURCE ( 'ANY', '', #7215, .NOT_KNOWN. ) ;
#19496=CYLINDRICAL_SURFACE ( 'NONE', #1655, 2.500000000000000444 ) ;
#19567=AXIS2_PLACEMENT_3D ( 'NONE', #20150, #296, #2329 ) ;
#19592=APPLICATION_CONTEXT ( 'configuration controlled 3d designs of mechanical parts and assemblies' ) ;
#19850=DIRECTION ( 'NONE',  ( -0.07397971354964476276, -0.9972597464969256142, 2.428612866367529538E-15 ) ) ;
#19938=CIRCLE ( 'NONE', #19567, 5.000000000000000000 ) ;
#19943=DIRECTION ( 'NONE',  ( 4.027614241767943373E-31, 2.300154215587010080E-15, 1.000000000000000000 ) ) ;
#19969=PLANE ( 'NONE',  #12024 ) ;
#20150=CARTESIAN_POINT ( 'NONE',  ( -20.00000000397270128, 22.95208919256889857, -5.499999999995559996 ) ) ;
#20390=CARTESIAN_POINT ( 'NONE',  ( -20.00000000397270128, 22.95208919256889857, -4.999999999995559996 ) ) ;
#20564=EDGE_LOOP ( 'NONE', ( #17038, #12731, #7789, #10108 ) ) ;
#20568=ORIENTED_EDGE ( 'NONE', *, *, #10005, .T. ) ;
#20612=VERTEX_POINT ( 'NONE', #21529 ) ;
#20894=AXIS2_PLACEMENT_3D ( 'NONE', #20390, #6908, #10482 ) ;
#20928=DIRECTION ( 'NONE',  ( -1.751019220569994795E-16, -2.300154215587015208E-15, -1.000000000000000000 ) ) ;
#21054=DIRECTION ( 'NONE',  ( -0.07397971354964476276, -0.9972597464969256142, 2.428612866367529538E-15 ) ) ;
#21063=CARTESIAN_POINT ( 'NONE',  ( -20.36989857172092044, 17.96579046008427127, -5.499999999995548450 ) ) ;
#21067=CARTESIAN_POINT ( 'NONE',  ( -20.00000000397270128, 22.95208919256889857, -5.499999999995559996 ) ) ;
#21107=EDGE_CURVE ( 'NONE', #3684, #20612, #2402, .T. ) ;
#21249=ADVANCED_FACE ( 'NONE', ( #12958, #9164 ), #19969, .F. ) ;
#21483=AXIS2_PLACEMENT_3D ( 'NONE', #6820, #8600, #13829 ) ;
#21529=CARTESIAN_POINT ( 'NONE',  ( -19.81505072009858992, 25.44523855881121577, -4.999999999995566213 ) ) ;
#21714=FACE_OUTER_BOUND ( 'NONE', #360, .T. ) ;
#21824=CARTESIAN_POINT ( 'NONE',  ( -20.00000000397270128, 22.95208919256889857, -4.999999999995559996 ) ) ;
#22104=EDGE_LOOP ( 'NONE', ( #8552, #16252, #7783, #6431 ) ) ;
#22226=DIRECTION ( 'NONE',  ( -1.751019220569994795E-16, -2.300154215587015208E-15, -1.000000000000000000 ) ) ;
#22243=CARTESIAN_POINT ( 'NONE',  ( -20.00000000397270128, 22.95208919256889857, -4.999999999995559996 ) ) ;
#22308=CARTESIAN_POINT ( 'NONE',  ( -19.63010143622448211, 27.93838792505352941, -5.499999999995570654 ) ) ;
#22702=( NAMED_UNIT ( * ) SI_UNIT ( $, .STERADIAN. ) SOLID_ANGLE_UNIT ( ) );
#23069=DIRECTION ( 'NONE',  ( -0.07397971354964408275, -0.9972597464969258363, 2.255140518769849223E-15 ) ) ;
#23456=SHAPE_DEFINITION_REPRESENTATION ( #17433, #5493 ) ;
#23543=COLOUR_RGB('Light Gray', 0.72549020, 0.75294118, 0.79215686);
#23544=FILL_AREA_STYLE_COLOUR('',#23543);
#23545=FILL_AREA_STYLE('',(#23544));
#23546=SURFACE_STYLE_FILL_AREA(#23545);
#23547=SURFACE_SIDE_STYLE('',(#23546));
#23548=SURFACE_STYLE_USAGE(.BOTH.,#23547);
#23549=PRESENTATION_STYLE_ASSIGNMENT((#23548));
#23563=STYLED_ITEM('',(#23549),#17389);
#23564=MECHANICAL_DESIGN_GEOMETRIC_PRESENTATION_REPRESENTATION('',(#23563),#10500);
ENDSEC;
END-ISO-10303-21;
